ISO-10303-21;
HEADER;
FILE_DESCRIPTION (('STEP AP214'),
    '1' );
FILE_NAME ('hex nut style 1_am_B18.2.4.1M - Hex nut, Style 1,  M10 x 1.5, with 16mm WAF --D-N__PD7643.step',
    '2026-10-24T15:53:57',
    ( '' ),
    ( '' ),
    'SwSTEP 2.0',
    'SolidWorks 2025',
    '' );
FILE_SCHEMA (( 'AUTOMOTIVE_DESIGN' ));
ENDSEC;

DATA;
#6=CARTESIAN_POINT ( 'NONE',  ( -8.000000000000229150, -4.618802153516843312, -0.7145311798163467287 ) ) ;
#17=CARTESIAN_POINT ( 'NONE',  ( -1.310872448938785073, 8.480771745766666925, -8.082649155111145234 ) ) ;
#36=VECTOR ( 'NONE', #1214, 1000.000000000000000 ) ;
#56=MANIFOLD_SOLID_BREP ( 'EndChamfer', #2646 ) ;
#64=CARTESIAN_POINT ( 'NONE',  ( 5.354491962337593947, -6.146186931204438153, -8.331901280394781395 ) ) ;
#74=CARTESIAN_POINT ( 'NONE',  ( -5.354491962338943090, 6.146186931204643322, -0.06809871960584383543 ) ) ;
#77=CARTESIAN_POINT ( 'NONE',  ( 8.000000000000007105, 0.000000000000000000, -8.400000000000018119 ) ) ;
#94=ORIENTED_EDGE ( 'NONE', *, *, #3041, .F. ) ;
#99=CARTESIAN_POINT ( 'NONE',  ( -6.689127551062222565, -5.375634714784565560, -0.3173508448887311095 ) ) ;
#135=EDGE_LOOP ( 'NONE', ( #1045, #4350, #4597 ) ) ;
#156=CARTESIAN_POINT ( 'NONE',  ( 3.999999999999337419, -6.928203230275431501, 0.000000000000000000 ) ) ;
#160=CARTESIAN_POINT ( 'NONE',  ( -8.000000000000666134, -3.867591403078895596, -0.4976753153248583139 ) ) ;
#161=ORIENTED_EDGE ( 'NONE', *, *, #1345, .T. ) ;
#170=EDGE_LOOP ( 'NONE', ( #1899, #7245, #7698, #4667, #2525, #5079 ) ) ;
#197=ADVANCED_FACE ( 'NONE', ( #1042 ), #6035, .F. ) ;
#198=ORIENTED_EDGE ( 'NONE', *, *, #1594, .T. ) ;
#202=CARTESIAN_POINT ( 'NONE',  ( 1.310872448937509205, -8.480771745766409353, -0.3173508448886196431 ) ) ;
#221=AXIS2_PLACEMENT_3D ( 'NONE', #2814, #2077, #2895 ) ;
#233=CARTESIAN_POINT ( 'NONE',  ( -5.080504117408889186, -2.106769544347818268, -8.400000000000018119 ) ) ;
#281=DIRECTION ( 'NONE',  ( 0.000000000000000000, 0.000000000000000000, -1.000000000000000000 ) ) ;
#289=CARTESIAN_POINT ( 'NONE',  ( 0.000000000000000000, 0.000000000000000000, -8.400000000000018119 ) ) ;
#322=CARTESIAN_POINT ( 'NONE',  ( -6.661338147750939243E-13, 9.237604307034352757, -0.7145311798163467287 ) ) ;
#349=EDGE_LOOP ( 'NONE', ( #8567, #7079, #5619, #6305, #3841, #1034 ) ) ;
#366=SHAPE_DEFINITION_REPRESENTATION ( #7163, #2397 ) ;
#374=CONICAL_SURFACE ( 'NONE', #5238, 8.000000000000007105, 1.047197551196597631 ) ;
#395=CARTESIAN_POINT ( 'NONE',  ( 8.000000000000012434, 0.7809653281576667272, -8.400000000000012790 ) ) ;
#418=CONICAL_SURFACE ( 'NONE', #3188, 8.000000000000007105, 1.047197551196597631 ) ;
#434=CARTESIAN_POINT ( 'NONE',  ( 7.999999999999340972, -4.618802153516732290, -7.685468820183672278 ) ) ;
#438=ORIENTED_EDGE ( 'NONE', *, *, #4062, .T. ) ;
#451=CARTESIAN_POINT ( 'NONE',  ( -8.000000000000673239, 4.618802153517287401, -7.685468820183672278 ) ) ;
#469=CARTESIAN_POINT ( 'NONE',  ( -8.000000000000229150, 4.440892098500626162E-13, -8.400000000000018119 ) ) ;
#470=FACE_OUTER_BOUND ( 'NONE', #349, .T. ) ;
#491=PLANE ( 'NONE',  #5476 ) ;
#523=CARTESIAN_POINT ( 'NONE',  ( -4.339467034331338624, -6.732211846623388674, -8.399999999999982592 ) ) ;
#525=CARTESIAN_POINT ( 'NONE',  ( -8.000000000000229150, 4.440892098500626162E-13, -8.400000000000018119 ) ) ;
#537=DIRECTION ( 'NONE',  ( 0.8660254037844367092, -0.5000000000000033307, 0.000000000000000000 ) ) ;
#540=PRODUCT_DEFINITION_CONTEXT ( 'detailed design', #5188, 'design' ) ;
#543=PLANE ( 'NONE',  #4683 ) ;
#547=ORIENTED_EDGE ( 'NONE', *, *, #2475, .T. ) ;
#574=ORIENTED_EDGE ( 'NONE', *, *, #8507, .T. ) ;
#597=CARTESIAN_POINT ( 'NONE',  ( -4.000000000000891731, 6.928203230275542523, -8.400000000000018119 ) ) ;
#613=CARTESIAN_POINT ( 'NONE',  ( -8.000000000000673239, 4.618802153517287401, -0.7145311798163467287 ) ) ;
#637=DIRECTION ( 'NONE',  ( 0.000000000000000000, 0.000000000000000000, 1.000000000000000000 ) ) ;
#661=( NAMED_UNIT ( * ) SI_UNIT ( $, .STERADIAN. ) SOLID_ANGLE_UNIT ( ) );
#669=( NAMED_UNIT ( * ) PLANE_ANGLE_UNIT ( ) SI_UNIT ( $, .RADIAN. ) );
#673=ADVANCED_FACE ( 'NONE', ( #2459 ), #4086, .T. ) ;
#677=B_SPLINE_CURVE_WITH_KNOTS ( 'NONE', 3,
 ( #1730, #6481, #3131, #8524, #3748, #2565 ),
 .UNSPECIFIED., .F., .F.,
 ( 4, 2, 4 ),
 ( 2.380731628247534354E-07, 0.002336973833157795794, 0.004673709593152765469 ),
 .UNSPECIFIED. ) ;
#688=CIRCLE ( 'NONE', #5560, 8.000000000000007105 ) ;
#703=DIRECTION ( 'NONE',  ( 0.000000000000000000, 0.000000000000000000, 1.000000000000000000 ) ) ;
#723=CARTESIAN_POINT ( 'NONE',  ( -8.000000000000671463, 3.871967595402323603, -0.4989386132328571533 ) ) ;
#725=CARTESIAN_POINT ( 'NONE',  ( -4.339467034331342177, -6.732211846623386897, -3.613251970573713029E-14 ) ) ;
#726=ORIENTED_EDGE ( 'NONE', *, *, #4374, .T. ) ;
#753=ADVANCED_FACE ( 'NONE', ( #6740 ), #2810, .F. ) ;
#767=FACE_OUTER_BOUND ( 'NONE', #135, .T. ) ;
#789=FACE_OUTER_BOUND ( 'NONE', #5636, .T. ) ;
#839=ORIENTED_EDGE ( 'NONE', *, *, #2260, .T. ) ;
#853=( GEOMETRIC_REPRESENTATION_CONTEXT ( 3 ) GLOBAL_UNCERTAINTY_ASSIGNED_CONTEXT ( ( #3952 ) ) GLOBAL_UNIT_ASSIGNED_CONTEXT ( ( #3224, #1825, #661 ) ) REPRESENTATION_CONTEXT ( 'NONE', 'WORKASPACE' ) );
#854=EDGE_CURVE ( 'NONE', #1579, #3453, #8518, .T. ) ;
#855=FACE_OUTER_BOUND ( 'NONE', #3407, .T. ) ;
#858=DIRECTION ( 'NONE',  ( 0.000000000000000000, 0.000000000000000000, 1.000000000000000000 ) ) ;
#871=CARTESIAN_POINT ( 'NONE',  ( -8.000000000000666134, -3.098204225877952744, -0.3157906771921843991 ) ) ;
#881=ORIENTED_EDGE ( 'NONE', *, *, #7417, .F. ) ;
#887=ORIENTED_EDGE ( 'NONE', *, *, #7094, .T. ) ;
#892=CARTESIAN_POINT ( 'NONE',  ( -5.080504117408895404, -2.106769544347820933, -8.400999999999992696 ) ) ;
#895=CARTESIAN_POINT ( 'NONE',  ( 0.000000000000000000, 0.000000000000000000, -8.400999999999992696 ) ) ;
#903=DIRECTION ( 'NONE',  ( 0.000000000000000000, 0.000000000000000000, -1.000000000000000000 ) ) ;
#914=CARTESIAN_POINT ( 'NONE',  ( 8.000000000000012434, -0.7805016046290649268, -6.776263578034402713E-15 ) ) ;
#921=CARTESIAN_POINT ( 'NONE',  ( -7.345652830559441071, 4.996589667937682222, -7.903584543330798518 ) ) ;
#931=CIRCLE ( 'NONE', #2743, 8.000000000000007105 ) ;
#932=LINE ( 'NONE', #892, #3752 ) ;
#973=CIRCLE ( 'NONE', #8341, 8.000000000000007105 ) ;
#974=FACE_OUTER_BOUND ( 'NONE', #4758, .T. ) ;
#977=ORIENTED_EDGE ( 'NONE', *, *, #5273, .T. ) ;
#990=CARTESIAN_POINT ( 'NONE',  ( 8.000000000000007105, 0.000000000000000000, 0.000000000000000000 ) ) ;
#993=CIRCLE ( 'NONE', #5875, 8.000000000000007105 ) ;
#995=EDGE_LOOP ( 'NONE', ( #6771, #4135, #161 ) ) ;
#1019=CARTESIAN_POINT ( 'NONE',  ( 6.689127551061982757, 5.375634714784596646, -0.3173508448886342426 ) ) ;
#1034=ORIENTED_EDGE ( 'NONE', *, *, #6568, .F. ) ;
#1042=FACE_OUTER_BOUND ( 'NONE', #170, .T. ) ;
#1044=DIRECTION ( 'NONE',  ( -1.000000000000000000, -8.881784197001244435E-16, -0.000000000000000000 ) ) ;
#1045=ORIENTED_EDGE ( 'NONE', *, *, #8248, .T. ) ;
#1050=PRODUCT ( 'hex nut style 1_am_B18.2.4.1M - Hex nut, Style 1,  M10 x 1.5, with 16mm WAF --D-N', 'hex nut style 1_am_B18.2.4.1M - Hex nut, Style 1,  M10 x 1.5, with 16mm WAF --D-N', '', ( #2446 ) ) ;
#1076=CARTESIAN_POINT ( 'NONE',  ( 4.000000000000003553, 6.928203230275431501, -8.400000000000018119 ) ) ;
#1079=CARTESIAN_POINT ( 'NONE',  ( -0.6543471694415553541, -8.859816792613555592, -0.4964154566687579706 ) ) ;
#1083=CARTESIAN_POINT ( 'NONE',  ( 8.000000000000007105, 0.000000000000000000, 0.000000000000000000 ) ) ;
#1097=CARTESIAN_POINT ( 'NONE',  ( -4.440892098500626162E-13, -9.237604307034018802, -7.685468820183672278 ) ) ;
#1115=DIRECTION ( 'NONE',  ( 0.000000000000000000, 0.000000000000000000, 1.000000000000000000 ) ) ;
#1134=DIRECTION ( 'NONE',  ( 0.8660254037844369313, 0.5000000000000028866, 0.000000000000000000 ) ) ;
#1137=DIRECTION ( 'NONE',  ( 0.000000000000000000, 0.000000000000000000, 1.000000000000000000 ) ) ;
#1147=EDGE_LOOP ( 'NONE', ( #2427, #2249, #1617 ) ) ;
#1152=UNCERTAINTY_MEASURE_WITH_UNIT (LENGTH_MEASURE( 1.000000000000000082E-05 ), #5243, 'distance_accuracy_value', 'NONE');
#1159=CARTESIAN_POINT ( 'NONE',  ( 5.354491962337593947, -6.146186931204438153, -0.06809871960523644630 ) ) ;
#1169=ORIENTED_EDGE ( 'NONE', *, *, #5273, .F. ) ;
#1174=CARTESIAN_POINT ( 'NONE',  ( -4.440892098500626162E-13, -9.237604307034018802, -0.7145311798163467287 ) ) ;
#1178=CARTESIAN_POINT ( 'NONE',  ( -0.6527133886637680460, 8.860760056386036254, -7.903039949738070113 ) ) ;
#1180=CARTESIAN_POINT ( 'NONE',  ( 2.644994884458577555, -7.710515798486396122, -8.317753204360382568 ) ) ;
#1187=DIRECTION ( 'NONE',  ( -0.000000000000000000, -0.000000000000000000, 1.000000000000000000 ) ) ;
#1190=EDGE_CURVE ( 'NONE', #6484, #5439, #6552, .T. ) ;
#1195=CARTESIAN_POINT ( 'NONE',  ( 8.000000000000008882, 1.572549600175702444, -0.06894455525514735228 ) ) ;
#1211=ORIENTED_EDGE ( 'NONE', *, *, #2083, .T. ) ;
#1214=DIRECTION ( 'NONE',  ( 0.000000000000000000, 0.000000000000000000, 1.000000000000000000 ) ) ;
#1231=B_SPLINE_CURVE_WITH_KNOTS ( 'NONE', 3,
 ( #6988, #7586, #1692, #6454, #2970, #1019, #4366, #1611 ),
 .UNSPECIFIED., .F., .F.,
 ( 4, 2, 2, 4 ),
 ( 0.004673709593152763735, 0.005837709341828114379, 0.007001709090503465890, 0.009329708587854167179 ),
 .UNSPECIFIED. ) ;
#1236=CARTESIAN_POINT ( 'NONE',  ( 0.000000000000000000, 0.000000000000000000, 0.000000000000000000 ) ) ;
#1239=CARTESIAN_POINT ( 'NONE',  ( 8.000000000000007105, 0.000000000000000000, -8.400000000000018119 ) ) ;
#1249=DIRECTION ( 'NONE',  ( 1.000000000000000000, 8.881784197001244435E-16, 0.000000000000000000 ) ) ;
#1281=ORIENTED_EDGE ( 'NONE', *, *, #854, .F. ) ;
#1291=ORIENTED_EDGE ( 'NONE', *, *, #5574, .F. ) ;
#1345=EDGE_CURVE ( 'NONE', #6377, #4401, #7869, .T. ) ;
#1361=ADVANCED_BREP_SHAPE_REPRESENTATION ( '', ( #56, #7563 ), #3397 ) ;
#1379=FACE_OUTER_BOUND ( 'NONE', #3507, .T. ) ;
#1384=VECTOR ( 'NONE', #3647, 1000.000000000000000 ) ;
#1385=CARTESIAN_POINT ( 'NONE',  ( 7.999999999999340972, -4.618802153516732290, -7.685468820183672278 ) ) ;
#1428=LINE ( 'NONE', #6063, #1853 ) ;
#1477=CARTESIAN_POINT ( 'NONE',  ( -8.000000000000229150, -4.618802153516843312, -0.7145311798163467287 ) ) ;
#1480=EDGE_CURVE ( 'NONE', #1856, #6375, #5530, .T. ) ;
#1491=EDGE_LOOP ( 'NONE', ( #7153, #7215, #3256 ) ) ;
#1521=ORIENTED_EDGE ( 'NONE', *, *, #6568, .T. ) ;
#1525=B_SPLINE_CURVE_WITH_KNOTS ( 'NONE', 3,
 ( #3559, #4032, #6228, #6101, #723, #2205 ),
 .UNSPECIFIED., .F., .F.,
 ( 4, 2, 4 ),
 ( 0.01291313371729497020, 0.01525081363757335544, 0.01758849355785174068 ),
 .UNSPECIFIED. ) ;
#1532=ADVANCED_FACE ( 'NONE', ( #4988 ), #543, .T. ) ;
#1533=CARTESIAN_POINT ( 'NONE',  ( 0.000000000000000000, 0.000000000000000000, -8.400000000000018119 ) ) ;
#1539=MECHANICAL_DESIGN_GEOMETRIC_PRESENTATION_REPRESENTATION('',(#5449),#853);
#1545=ADVANCED_FACE ( 'NONE', ( #2332 ), #374, .T. ) ;
#1572=CARTESIAN_POINT ( 'NONE',  ( -3.319543390096983071, 7.321065037175590540, -0.01688885742807798990 ) ) ;
#1579=VERTEX_POINT ( 'NONE', #2421 ) ;
#1580=CARTESIAN_POINT ( 'NONE',  ( 0.000000000000000000, 0.000000000000000000, 0.000000000000000000 ) ) ;
#1587=CARTESIAN_POINT ( 'NONE',  ( 8.000000000000007105, 4.618802153516954334, -8.400000000000018119 ) ) ;
#1589=VERTEX_POINT ( 'NONE', #1076 ) ;
#1594=EDGE_CURVE ( 'NONE', #6377, #8133, #7604, .T. ) ;
#1598=CARTESIAN_POINT ( 'NONE',  ( 0.000000000000000000, 0.000000000000000000, -8.400000000000018119 ) ) ;
#1605=CARTESIAN_POINT ( 'NONE',  ( -5.354491962338943090, 6.146186931204643322, -8.331901280394173881 ) ) ;
#1608=EDGE_CURVE ( 'NONE', #7519, #2221, #931, .T. ) ;
#1611=CARTESIAN_POINT ( 'NONE',  ( 8.000000000000007105, 4.618802153517065356, -0.7145311798163467287 ) ) ;
#1617=ORIENTED_EDGE ( 'NONE', *, *, #4404, .F. ) ;
#1643=EDGE_LOOP ( 'NONE', ( #4815, #7980, #4430 ) ) ;
#1648=CARTESIAN_POINT ( 'NONE',  ( -3.660532965669702321, 7.124194613927820718, -3.312531980892385906E-13 ) ) ;
#1665=ORIENTED_EDGE ( 'NONE', *, *, #1608, .T. ) ;
#1691=CARTESIAN_POINT ( 'NONE',  ( -8.000000000000667910, -3.098204225877948303, -8.084209322807835107 ) ) ;
#1692=CARTESIAN_POINT ( 'NONE',  ( 4.680456609903965948, 6.535341423375566450, -0.01688885742775289925 ) ) ;
#1698=B_SPLINE_CURVE_WITH_KNOTS ( 'NONE', 3,
 ( #3700, #1079, #6364, #3738, #3076, #4466 ),
 .UNSPECIFIED., .F., .F.,
 ( 4, 2, 4 ),
 ( 2.380731626890316258E-07, 0.002336973833157048996, 0.004673709593151410650 ),
 .UNSPECIFIED. ) ;
#1701=AXIS2_PLACEMENT_3D ( 'NONE', #5473, #2240, #6910 ) ;
#1719=DIRECTION ( 'NONE',  ( 0.000000000000000000, 0.000000000000000000, 1.000000000000000000 ) ) ;
#1730=CARTESIAN_POINT ( 'NONE',  ( -6.661338147750939243E-13, 9.237604307034352757, -7.685468820183672278 ) ) ;
#1741=DIRECTION ( 'NONE',  ( 1.000000000000000000, 8.881784197001244435E-16, 0.000000000000000000 ) ) ;
#1772=CIRCLE ( 'NONE', #6248, 8.000000000000007105 ) ;
#1786=APPLICATION_CONTEXT ( 'automotive_design' ) ;
#1809=PLANE ( 'NONE',  #2954 ) ;
#1813=CARTESIAN_POINT ( 'NONE',  ( 7.345652830558279334, -4.996589667937374024, -0.4964154566685609615 ) ) ;
#1825=( NAMED_UNIT ( * ) PLANE_ANGLE_UNIT ( ) SI_UNIT ( $, .RADIAN. ) );
#1827=CONICAL_SURFACE ( 'NONE', #7254, 8.000000000000007105, 1.047197551196597631 ) ;
#1833=ADVANCED_FACE ( 'NONE', ( #855 ), #6492, .T. ) ;
#1849=DIRECTION ( 'NONE',  ( 0.000000000000000000, 0.000000000000000000, 1.000000000000000000 ) ) ;
#1853=VECTOR ( 'NONE', #637, 1000.000000000000000 ) ;
#1856=VERTEX_POINT ( 'NONE', #4248 ) ;
#1864=CARTESIAN_POINT ( 'NONE',  ( 8.000000000000007105, 4.618802153517065356, -7.685468820183672278 ) ) ;
#1869=DIRECTION ( 'NONE',  ( -1.000000000000000000, -8.881784197001244435E-16, 0.000000000000000000 ) ) ;
#1899=ORIENTED_EDGE ( 'NONE', *, *, #2809, .F. ) ;
#1902=DIRECTION ( 'NONE',  ( 0.000000000000000000, 0.000000000000000000, -1.000000000000000000 ) ) ;
#1912=EDGE_CURVE ( 'NONE', #1589, #5078, #1772, .T. ) ;
#1913=ORIENTED_EDGE ( 'NONE', *, *, #2767, .T. ) ;
#1931=AXIS2_PLACEMENT_3D ( 'NONE', #2061, #6542, #8583 ) ;
#1938=FACE_OUTER_BOUND ( 'NONE', #1643, .T. ) ;
#1964=CARTESIAN_POINT ( 'NONE',  ( 0.000000000000000000, 0.000000000000000000, -8.400000000000018119 ) ) ;
#1983=AXIS2_PLACEMENT_3D ( 'NONE', #5865, #3832, #4580 ) ;
#2021=CARTESIAN_POINT ( 'NONE',  ( 5.690023276062378343, 5.952467836904126841, -8.269346954796224836 ) ) ;
#2061=CARTESIAN_POINT ( 'NONE',  ( 0.000000000000000000, 0.000000000000000000, -8.400000000000018119 ) ) ;
#2077=DIRECTION ( 'NONE',  ( 0.000000000000000000, 0.000000000000000000, -1.000000000000000000 ) ) ;
#2083=EDGE_CURVE ( 'NONE', #5384, #4294, #3684, .T. ) ;
#2092=CARTESIAN_POINT ( 'NONE',  ( -3.319543390096982183, 7.321065037175590540, -8.383111142571939567 ) ) ;
#2094=AXIS2_PLACEMENT_3D ( 'NONE', #7176, #2598, #8004 ) ;
#2119=EDGE_CURVE ( 'NONE', #6993, #6484, #5717, .T. ) ;
#2122=VERTEX_POINT ( 'NONE', #5877 ) ;
#2148=DIRECTION ( 'NONE',  ( 0.9237280213470678847, 0.3830490080632384942, 0.000000000000000000 ) ) ;
#2162=ORIENTED_EDGE ( 'NONE', *, *, #4374, .F. ) ;
#2177=CARTESIAN_POINT ( 'NONE',  ( 3.319543390095492263, -7.321065037175465307, -0.01688885742765811049 ) ) ;
#2187=CARTESIAN_POINT ( 'NONE',  ( -4.000000000000891731, 6.928203230275542523, -8.400000000000018119 ) ) ;
#2205=CARTESIAN_POINT ( 'NONE',  ( -8.000000000000673239, 4.618802153517287401, -0.7145311798163467287 ) ) ;
#2221=VERTEX_POINT ( 'NONE', #6776 ) ;
#2223=ORIENTED_EDGE ( 'NONE', *, *, #3549, .T. ) ;
#2230=ORIENTED_EDGE ( 'NONE', *, *, #3361, .T. ) ;
#2235=B_SPLINE_CURVE_WITH_KNOTS ( 'NONE', 3,
 ( #4881, #921, #6291, #1605, #7496, #2187 ),
 .UNSPECIFIED., .F., .F.,
 ( 4, 2, 4 ),
 ( 2.380731626810059357E-07, 0.002336973833157153079, 0.004673709593151625756 ),
 .UNSPECIFIED. ) ;
#2240=DIRECTION ( 'NONE',  ( 0.000000000000000000, 0.000000000000000000, 1.000000000000000000 ) ) ;
#2245=ORIENTED_EDGE ( 'NONE', *, *, #5821, .F. ) ;
#2249=ORIENTED_EDGE ( 'NONE', *, *, #5574, .T. ) ;
#2256=PLANE ( 'NONE',  #6146 ) ;
#2260=EDGE_CURVE ( 'NONE', #2221, #2870, #1231, .T. ) ;
#2274=ORIENTED_EDGE ( 'NONE', *, *, #4833, .F. ) ;
#2297=DIRECTION ( 'NONE',  ( 0.000000000000000000, 0.000000000000000000, -1.000000000000000000 ) ) ;
#2313=VERTEX_POINT ( 'NONE', #5784 ) ;
#2331=EDGE_CURVE ( 'NONE', #6484, #1589, #688, .T. ) ;
#2332=FACE_OUTER_BOUND ( 'NONE', #3534, .T. ) ;
#2336=VERTEX_POINT ( 'NONE', #8417 ) ;
#2363=AXIS2_PLACEMENT_3D ( 'NONE', #5654, #1137, #3798 ) ;
#2397=SHAPE_REPRESENTATION ( 'hex nut style 1_am_B18.2.4.1M - Hex nut, Style 1,  M10 x 1.5, with 16mm WAF --D-N', ( #7563 ), #3397 ) ;
#2411=CARTESIAN_POINT ( 'NONE',  ( -6.661338147750939243E-13, 9.237604307034352757, -8.400000000000018119 ) ) ;
#2421=CARTESIAN_POINT ( 'NONE',  ( -5.080504117408895404, -2.106769544347820933, 0.000000000000000000 ) ) ;
#2427=ORIENTED_EDGE ( 'NONE', *, *, #5571, .F. ) ;
#2446=PRODUCT_CONTEXT ( 'NONE', #1786, 'mechanical' ) ;
#2459=FACE_OUTER_BOUND ( 'NONE', #1147, .T. ) ;
#2460=DIRECTION ( 'NONE',  ( 1.000000000000000000, 8.881784197001244435E-16, 0.000000000000000000 ) ) ;
#2475=EDGE_CURVE ( 'NONE', #4132, #1579, #932, .T. ) ;
#2506=DIRECTION ( 'NONE',  ( -1.000000000000000000, -8.881784197001244435E-16, 0.000000000000000000 ) ) ;
#2525=ORIENTED_EDGE ( 'NONE', *, *, #7464, .T. ) ;
#2527=EDGE_CURVE ( 'NONE', #4401, #6993, #973, .T. ) ;
#2531=CARTESIAN_POINT ( 'NONE',  ( 7.999999999999340972, -4.618802153516732290, -8.400000000000018119 ) ) ;
#2544=AXIS2_PLACEMENT_3D ( 'NONE', #8108, #3446, #2148 ) ;
#2545=CARTESIAN_POINT ( 'NONE',  ( 3.318518101602916381, 7.321656987762904301, 1.790627650495590601E-14 ) ) ;
#2556=CARTESIAN_POINT ( 'NONE',  ( 8.000000000000015987, -3.867591403078991519, -7.902324684675471111 ) ) ;
#2563=CARTESIAN_POINT ( 'NONE',  ( 8.000000000000007105, 0.000000000000000000, -8.400000000000018119 ) ) ;
#2564=ORIENTED_EDGE ( 'NONE', *, *, #7429, .F. ) ;
#2565=CARTESIAN_POINT ( 'NONE',  ( 4.000000000000003553, 6.928203230275431501, -8.400000000000018119 ) ) ;
#2588=PLANE ( 'NONE',  #2687 ) ;
#2598=DIRECTION ( 'NONE',  ( 0.000000000000000000, 0.000000000000000000, -1.000000000000000000 ) ) ;
#2646=CLOSED_SHELL ( 'NONE', ( #5216, #5927, #8119, #197, #6352, #3334, #1532, #8317, #7724, #4958, #6191, #1545, #6666, #8096, #6498, #5080, #6288, #1833, #5942, #5098, #673, #753 ) ) ;
#2657=CONICAL_SURFACE ( 'NONE', #2363, 8.000000000000007105, 1.047197551196597631 ) ;
#2664=CARTESIAN_POINT ( 'NONE',  ( -4.680456609904129373, -6.535341423375579772, -8.383111142572207797 ) ) ;
#2665=AXIS2_PLACEMENT_3D ( 'NONE', #3637, #7028, #3719 ) ;
#2667=EDGE_CURVE ( 'NONE', #6993, #8513, #5190, .T. ) ;
#2669=ORIENTED_EDGE ( 'NONE', *, *, #6166, .F. ) ;
#2687=AXIS2_PLACEMENT_3D ( 'NONE', #7204, #6504, #537 ) ;
#2700=CARTESIAN_POINT ( 'NONE',  ( -6.661338147750939243E-13, 9.237604307034352757, -7.685468820183672278 ) ) ;
#2715=ORIENTED_EDGE ( 'NONE', *, *, #2809, .T. ) ;
#2737=EDGE_LOOP ( 'NONE', ( #8037, #4902, #6393 ) ) ;
#2743=AXIS2_PLACEMENT_3D ( 'NONE', #7812, #1849, #5030 ) ;
#2767=EDGE_CURVE ( 'NONE', #4141, #4545, #4463, .T. ) ;
#2769=CARTESIAN_POINT ( 'NONE',  ( -0.6527133886637689342, 8.860760056386036254, -0.4969600502619508364 ) ) ;
#2772=CARTESIAN_POINT ( 'NONE',  ( -5.355005115541064953, -6.145890662064632082, -0.08224679563976682040 ) ) ;
#2809=EDGE_CURVE ( 'NONE', #5902, #7519, #7584, .T. ) ;
#2810=CYLINDRICAL_SURFACE ( 'NONE', #1701, 5.500000000000023981 ) ;
#2814=CARTESIAN_POINT ( 'NONE',  ( 0.000000000000000000, 0.000000000000000000, 0.000000000000000000 ) ) ;
#2826=CARTESIAN_POINT ( 'NONE',  ( -4.000000000000891731, 6.928203230275542523, -8.400000000000018119 ) ) ;
#2854=CIRCLE ( 'NONE', #7716, 8.000000000000007105 ) ;
#2868=ORIENTED_EDGE ( 'NONE', *, *, #6386, .T. ) ;
#2870=VERTEX_POINT ( 'NONE', #4263 ) ;
#2891=B_SPLINE_CURVE_WITH_KNOTS ( 'NONE', 3,
 ( #5178, #5362, #8569, #6075, #6027, #7920 ),
 .UNSPECIFIED., .F., .F.,
 ( 4, 2, 4 ),
 ( 2.380731626890628072E-07, 0.002336973833157054200, 0.004673709593151418457 ),
 .UNSPECIFIED. ) ;
#2895=DIRECTION ( 'NONE',  ( -1.000000000000000000, -8.881784197001244435E-16, 0.000000000000000000 ) ) ;
#2899=ORIENTED_EDGE ( 'NONE', *, *, #2331, .T. ) ;
#2937=CARTESIAN_POINT ( 'NONE',  ( 0.000000000000000000, 0.000000000000000000, -8.400000000000018119 ) ) ;
#2954=AXIS2_PLACEMENT_3D ( 'NONE', #7903, #8550, #7383 ) ;
#2959=VERTEX_POINT ( 'NONE', #7738 ) ;
#2961=ORIENTED_EDGE ( 'NONE', *, *, #3356, .F. ) ;
#2962=B_SPLINE_CURVE_WITH_KNOTS ( 'NONE', 3,
 ( #7773, #5076, #1195, #5722, #7170, #5114 ),
 .UNSPECIFIED., .F., .F.,
 ( 4, 2, 4 ),
 ( 0.01291313371729433702, 0.01525081363757293043, 0.01758849355785152557 ),
 .UNSPECIFIED. ) ;
#2970=CARTESIAN_POINT ( 'NONE',  ( 5.690023276062378343, 5.952467836904126841, -0.1306530452037925616 ) ) ;
#2973=PLANE ( 'NONE',  #2665 ) ;
#2996=CARTESIAN_POINT ( 'NONE',  ( 3.999999999999337419, -6.928203230275431501, -8.400000000000018119 ) ) ;
#3032=CARTESIAN_POINT ( 'NONE',  ( -8.000000000000671463, 1.572549600175901618, -8.331055444744475125 ) ) ;
#3037=EDGE_LOOP ( 'NONE', ( #1291, #1169, #881, #8078, #1665, #94 ) ) ;
#3040=AXIS2_PLACEMENT_3D ( 'NONE', #4180, #8187, #1249 ) ;
#3041=EDGE_CURVE ( 'NONE', #2313, #2221, #993, .T. ) ;
#3047=ORIENTED_EDGE ( 'NONE', *, *, #7195, .F. ) ;
#3073=CARTESIAN_POINT ( 'NONE',  ( -8.000000000000667910, 0.7809653281580535289, -8.399999999999606004 ) ) ;
#3076=CARTESIAN_POINT ( 'NONE',  ( -3.318518101603131765, -7.321656987762887425, -3.464364754270089018E-14 ) ) ;
#3085=ORIENTED_EDGE ( 'NONE', *, *, #1190, .F. ) ;
#3086=AXIS2_PLACEMENT_3D ( 'NONE', #4302, #5579, #8227 ) ;
#3098=AXIS2_PLACEMENT_3D ( 'NONE', #1964, #703, #7279 ) ;
#3131=CARTESIAN_POINT ( 'NONE',  ( 1.313474075706796862, 8.479269695851089139, -8.083279549040090828 ) ) ;
#3145=EDGE_CURVE ( 'NONE', #8513, #4401, #2891, .T. ) ;
#3160=CARTESIAN_POINT ( 'NONE',  ( -8.000000000000673239, 3.871967595402326268, -7.901061386767160855 ) ) ;
#3177=CARTESIAN_POINT ( 'NONE',  ( -6.689127551062228783, -5.375634714784562895, -8.082649155111287342 ) ) ;
#3180=LINE ( 'NONE', #2531, #8114 ) ;
#3186=ORIENTED_EDGE ( 'NONE', *, *, #7417, .T. ) ;
#3188=AXIS2_PLACEMENT_3D ( 'NONE', #1236, #4691, #3895 ) ;
#3213=CARTESIAN_POINT ( 'NONE',  ( 7.345652830558279334, -4.996589667937374024, -7.903584543331455770 ) ) ;
#3224=( LENGTH_UNIT ( ) NAMED_UNIT ( * ) SI_UNIT ( .MILLI., .METRE. ) );
#3249=CARTESIAN_POINT ( 'NONE',  ( 4.681481898396449459, -6.534749472788188740, 1.717715054395940744E-13 ) ) ;
#3253=CARTESIAN_POINT ( 'NONE',  ( 0.000000000000000000, 0.000000000000000000, 0.000000000000000000 ) ) ;
#3256=ORIENTED_EDGE ( 'NONE', *, *, #2527, .T. ) ;
#3263=CARTESIAN_POINT ( 'NONE',  ( -6.686525924293513334, 5.377136764700441773, -0.3167204509602711826 ) ) ;
#3277=CARTESIAN_POINT ( 'NONE',  ( 8.000000000000007105, 4.618802153517065356, -7.685468820183672278 ) ) ;
#3285=CARTESIAN_POINT ( 'NONE',  ( -4.000000000000003553, -6.928203230275431501, 0.000000000000000000 ) ) ;
#3305=ORIENTED_EDGE ( 'NONE', *, *, #854, .T. ) ;
#3319=FACE_OUTER_BOUND ( 'NONE', #5588, .T. ) ;
#3322=CARTESIAN_POINT ( 'NONE',  ( 6.689127551061982757, 5.375634714784596646, -8.082649155111388595 ) ) ;
#3334=ADVANCED_FACE ( 'NONE', ( #5201 ), #2588, .T. ) ;
#3356=EDGE_CURVE ( 'NONE', #5078, #6377, #5904, .T. ) ;
#3361=EDGE_CURVE ( 'NONE', #4294, #2221, #5172, .T. ) ;
#3397=( GEOMETRIC_REPRESENTATION_CONTEXT ( 3 ) GLOBAL_UNCERTAINTY_ASSIGNED_CONTEXT ( ( #1152 ) ) GLOBAL_UNIT_ASSIGNED_CONTEXT ( ( #5243, #669, #6048 ) ) REPRESENTATION_CONTEXT ( 'NONE', 'WORKASPACE' ) );
#3407=EDGE_LOOP ( 'NONE', ( #2715, #3758, #5527 ) ) ;
#3409=VERTEX_POINT ( 'NONE', #5755 ) ;
#3418=ORIENTED_EDGE ( 'NONE', *, *, #6718, .F. ) ;
#3425=DIRECTION ( 'NONE',  ( 1.000000000000000000, 8.881784197001244435E-16, 0.000000000000000000 ) ) ;
#3446=DIRECTION ( 'NONE',  ( -0.000000000000000000, -0.000000000000000000, 1.000000000000000000 ) ) ;
#3453=VERTEX_POINT ( 'NONE', #8463 ) ;
#3467=CIRCLE ( 'NONE', #4019, 5.500000000000023981 ) ;
#3506=CARTESIAN_POINT ( 'NONE',  ( 0.000000000000000000, 0.000000000000000000, 0.000000000000000000 ) ) ;
#3507=EDGE_LOOP ( 'NONE', ( #977, #7262, #4281 ) ) ;
#3509=CARTESIAN_POINT ( 'NONE',  ( 0.000000000000000000, 0.000000000000000000, 0.000000000000000000 ) ) ;
#3512=DIRECTION ( 'NONE',  ( 1.000000000000000000, 0.000000000000000000, 0.000000000000000000 ) ) ;
#3522=FACE_BOUND ( 'NONE', #3597, .T. ) ;
#3534=EDGE_LOOP ( 'NONE', ( #2223, #3085, #2899 ) ) ;
#3538=CIRCLE ( 'NONE', #8401, 5.500000000000023981 ) ;
#3549=EDGE_CURVE ( 'NONE', #1589, #5439, #7366, .T. ) ;
#3553=CARTESIAN_POINT ( 'NONE',  ( 0.000000000000000000, 0.000000000000000000, 0.000000000000000000 ) ) ;
#3558=LINE ( 'NONE', #6185, #1384 ) ;
#3559=CARTESIAN_POINT ( 'NONE',  ( -8.000000000000229150, 4.440892098500626162E-13, 0.000000000000000000 ) ) ;
#3567=CARTESIAN_POINT ( 'NONE',  ( -4.440892098500626162E-13, -9.237604307034018802, -0.7145311798163467287 ) ) ;
#3591=CARTESIAN_POINT ( 'NONE',  ( -1.310872448938785739, 8.480771745766666925, -0.3173508448888719413 ) ) ;
#3597=EDGE_LOOP ( 'NONE', ( #1281, #4112 ) ) ;
#3611=CARTESIAN_POINT ( 'NONE',  ( -6.661338147750939243E-13, 9.237604307034352757, 0.000000000000000000 ) ) ;
#3634=CARTESIAN_POINT ( 'NONE',  ( -8.000000000000664357, -1.555946510855793052, -8.332911297836323783 ) ) ;
#3637=CARTESIAN_POINT ( 'NONE',  ( 8.000000000000007105, 4.618802153516954334, -8.400000000000018119 ) ) ;
#3647=DIRECTION ( 'NONE',  ( 0.000000000000000000, 0.000000000000000000, 1.000000000000000000 ) ) ;
#3666=FACE_OUTER_BOUND ( 'NONE', #7388, .T. ) ;
#3673=CARTESIAN_POINT ( 'NONE',  ( 0.000000000000000000, 0.000000000000000000, -8.400000000000018119 ) ) ;
#3680=CYLINDRICAL_SURFACE ( 'NONE', #6273, 5.500000000000023981 ) ;
#3684=LINE ( 'NONE', #2411, #6538 ) ;
#3700=CARTESIAN_POINT ( 'NONE',  ( -4.440892098500626162E-13, -9.237604307034018802, -0.7145311798163467287 ) ) ;
#3714=CARTESIAN_POINT ( 'NONE',  ( -8.000000000000007105, -4.618802153517065356, -8.400000000000018119 ) ) ;
#3715=CARTESIAN_POINT ( 'NONE',  ( -2.644994884460003526, 7.710515798486560435, -0.08224679563998771314 ) ) ;
#3719=DIRECTION ( 'NONE',  ( -0.8660254037844365982, 0.5000000000000035527, -0.000000000000000000 ) ) ;
#3738=CARTESIAN_POINT ( 'NONE',  ( -2.645508037662050338, -7.710219529346595380, -0.06809871960545571534 ) ) ;
#3748=CARTESIAN_POINT ( 'NONE',  ( 3.318518101602915493, 7.321656987762904301, -8.400000000000034106 ) ) ;
#3752=VECTOR ( 'NONE', #8290, 1000.000000000000000 ) ;
#3758=ORIENTED_EDGE ( 'NONE', *, *, #5341, .T. ) ;
#3780=CARTESIAN_POINT ( 'NONE',  ( 8.000000000000007105, 4.618802153517065356, -7.685468820183672278 ) ) ;
#3798=DIRECTION ( 'NONE',  ( 1.000000000000000000, 8.881784197001244435E-16, 0.000000000000000000 ) ) ;
#3819=CARTESIAN_POINT ( 'NONE',  ( 3.999999999999337419, -6.928203230275431501, 0.000000000000000000 ) ) ;
#3832=DIRECTION ( 'NONE',  ( 0.000000000000000000, 0.000000000000000000, -1.000000000000000000 ) ) ;
#3841=ORIENTED_EDGE ( 'NONE', *, *, #8248, .F. ) ;
#3895=DIRECTION ( 'NONE',  ( -1.000000000000000000, -8.881784197001244435E-16, 0.000000000000000000 ) ) ;
#3902=ORIENTED_EDGE ( 'NONE', *, *, #8462, .F. ) ;
#3913=CARTESIAN_POINT ( 'NONE',  ( -4.000000000000003553, -6.928203230275431501, -8.400000000000018119 ) ) ;
#3952=UNCERTAINTY_MEASURE_WITH_UNIT (LENGTH_MEASURE( 1.000000000000000082E-05 ), #3224, 'distance_accuracy_value', 'NONE');
#3981=CARTESIAN_POINT ( 'NONE',  ( 4.000000000000003553, 6.928203230275431501, -8.400000000000018119 ) ) ;
#3989=ORIENTED_EDGE ( 'NONE', *, *, #2119, .T. ) ;
#4014=CONICAL_SURFACE ( 'NONE', #3040, 8.000000000000007105, 1.047197551196597631 ) ;
#4019=AXIS2_PLACEMENT_3D ( 'NONE', #1598, #4260, #8353 ) ;
#4024=CARTESIAN_POINT ( 'NONE',  ( 4.680456609903968612, 6.535341423375565562, -8.383111142572266417 ) ) ;
#4032=CARTESIAN_POINT ( 'NONE',  ( -8.000000000000669687, 0.7809653281580556383, -4.133046444150523246E-13 ) ) ;
#4053=CARTESIAN_POINT ( 'NONE',  ( 0.000000000000000000, 0.000000000000000000, -8.400000000000018119 ) ) ;
#4062=EDGE_CURVE ( 'NONE', #3453, #1579, #3538, .T. ) ;
#4065=DIRECTION ( 'NONE',  ( -1.000000000000000000, -8.881784197001244435E-16, -0.000000000000000000 ) ) ;
#4071=DIRECTION ( 'NONE',  ( -0.9237280213470678847, -0.3830490080632384942, 0.000000000000000000 ) ) ;
#4076=CARTESIAN_POINT ( 'NONE',  ( -8.000000000000667910, -3.867591403078892487, -7.902324684675164690 ) ) ;
#4086=CONICAL_SURFACE ( 'NONE', #5477, 8.000000000000007105, 1.047197551196597631 ) ;
#4091=LINE ( 'NONE', #6023, #8415 ) ;
#4112=ORIENTED_EDGE ( 'NONE', *, *, #4062, .F. ) ;
#4120=ORIENTED_EDGE ( 'NONE', *, *, #4754, .F. ) ;
#4121=LINE ( 'NONE', #1587, #7919 ) ;
#4132=VERTEX_POINT ( 'NONE', #233 ) ;
#4135=ORIENTED_EDGE ( 'NONE', *, *, #6166, .T. ) ;
#4141=VERTEX_POINT ( 'NONE', #7382 ) ;
#4180=CARTESIAN_POINT ( 'NONE',  ( 0.000000000000000000, 0.000000000000000000, -8.400000000000018119 ) ) ;
#4189=DIRECTION ( 'NONE',  ( -0.000000000000000000, -0.000000000000000000, 1.000000000000000000 ) ) ;
#4203=CARTESIAN_POINT ( 'NONE',  ( 0.000000000000000000, 0.000000000000000000, 0.000000000000000000 ) ) ;
#4218=EDGE_LOOP ( 'NONE', ( #7272, #4714, #7917, #4120, #2274, #5116 ) ) ;
#4248=CARTESIAN_POINT ( 'NONE',  ( 3.999999999999337419, -6.928203230275431501, 0.000000000000000000 ) ) ;
#4260=DIRECTION ( 'NONE',  ( -0.000000000000000000, -0.000000000000000000, 1.000000000000000000 ) ) ;
#4263=CARTESIAN_POINT ( 'NONE',  ( 8.000000000000007105, 4.618802153517065356, -0.7145311798163467287 ) ) ;
#4270=ORIENTED_EDGE ( 'NONE', *, *, #2667, .F. ) ;
#4281=ORIENTED_EDGE ( 'NONE', *, *, #6751, .F. ) ;
#4294=VERTEX_POINT ( 'NONE', #322 ) ;
#4300=DIRECTION ( 'NONE',  ( 0.000000000000000000, 0.000000000000000000, -1.000000000000000000 ) ) ;
#4302=CARTESIAN_POINT ( 'NONE',  ( 8.000000000000007105, 4.618802153516954334, -8.400000000000018119 ) ) ;
#4349=CARTESIAN_POINT ( 'NONE',  ( 8.000000000000012434, -1.555946510856073273, -0.06708870216335555137 ) ) ;
#4350=ORIENTED_EDGE ( 'NONE', *, *, #6718, .T. ) ;
#4359=DIRECTION ( 'NONE',  ( 0.000000000000000000, 0.000000000000000000, -1.000000000000000000 ) ) ;
#4364=LINE ( 'NONE', #3714, #36 ) ;
#4365=CARTESIAN_POINT ( 'NONE',  ( -8.000000000000229150, 4.440892098500626162E-13, -8.400000000000018119 ) ) ;
#4366=CARTESIAN_POINT ( 'NONE',  ( 7.347286611336940609, 4.995646404165252186, -0.4969600502617288473 ) ) ;
#4369=CARTESIAN_POINT ( 'NONE',  ( 3.319543390095480717, -7.321065037175468859, -8.383111142572358787 ) ) ;
#4374=EDGE_CURVE ( 'NONE', #4132, #2959, #4643, .T. ) ;
#4386=B_SPLINE_CURVE_WITH_KNOTS ( 'NONE', 3,
 ( #2826, #5451, #2092, #7396, #7156, #17, #1178, #2700 ),
 .UNSPECIFIED., .F., .F.,
 ( 4, 2, 2, 4 ),
 ( 0.004673709593151625756, 0.005837709341827238343, 0.007001709090502850064, 0.009329708587854075238 ),
 .UNSPECIFIED. ) ;
#4394=CARTESIAN_POINT ( 'NONE',  ( 8.000000000000012434, -0.7805016046290643716, -8.400000000000012790 ) ) ;
#4401=VERTEX_POINT ( 'NONE', #3913 ) ;
#4404=EDGE_CURVE ( 'NONE', #3409, #2313, #4867, .T. ) ;
#4412=AXIS2_PLACEMENT_3D ( 'NONE', #4053, #6670, #8148 ) ;
#4420=CARTESIAN_POINT ( 'NONE',  ( 1.313474075706797528, 8.479269695851089139, -0.3167204509599274576 ) ) ;
#4430=ORIENTED_EDGE ( 'NONE', *, *, #2260, .F. ) ;
#4438=CONICAL_SURFACE ( 'NONE', #5567, 8.000000000000007105, 1.047197551196597631 ) ;
#4443=FACE_OUTER_BOUND ( 'NONE', #5817, .T. ) ;
#4451=CARTESIAN_POINT ( 'NONE',  ( 1.310872448937506096, -8.480771745766409353, -8.082649155111401029 ) ) ;
#4463=B_SPLINE_CURVE_WITH_KNOTS ( 'NONE', 3,
 ( #1477, #160, #871, #4793, #7452, #6664 ),
 .UNSPECIFIED., .F., .F.,
 ( 4, 2, 4 ),
 ( 0.008240550023493657672, 0.01057684187039431394, 0.01291313371729497020 ),
 .UNSPECIFIED. ) ;
#4466=CARTESIAN_POINT ( 'NONE',  ( -4.000000000000003553, -6.928203230275431501, 0.000000000000000000 ) ) ;
#4491=CARTESIAN_POINT ( 'NONE',  ( 3.999999999999337419, -6.928203230275431501, -8.400000000000018119 ) ) ;
#4503=DIRECTION ( 'NONE',  ( -1.000000000000000000, -2.824407374646398239E-13, 0.000000000000000000 ) ) ;
#4513=CARTESIAN_POINT ( 'NONE',  ( 7.999999999999340972, -4.618802153516732290, -0.7145311798163467287 ) ) ;
#4526=EDGE_LOOP ( 'NONE', ( #5063, #5971, #438, #7847 ) ) ;
#4533=B_SPLINE_CURVE_WITH_KNOTS ( 'NONE', 3,
 ( #1385, #3213, #4746, #64, #7392, #6754 ),
 .UNSPECIFIED., .F., .F.,
 ( 4, 2, 4 ),
 ( 2.380731632860738630E-07, 0.002336973833158035620, 0.004673709593152784551 ),
 .UNSPECIFIED. ) ;
#4543=DIRECTION ( 'NONE',  ( 0.000000000000000000, 0.000000000000000000, -1.000000000000000000 ) ) ;
#4545=VERTEX_POINT ( 'NONE', #7544 ) ;
#4580=DIRECTION ( 'NONE',  ( -1.000000000000000000, -8.881784197001244435E-16, 0.000000000000000000 ) ) ;
#4587=CONICAL_SURFACE ( 'NONE', #2094, 8.000000000000007105, 1.047197551196597631 ) ;
#4597=ORIENTED_EDGE ( 'NONE', *, *, #1912, .T. ) ;
#4643=CIRCLE ( 'NONE', #2544, 5.500000000000023981 ) ;
#4667=ORIENTED_EDGE ( 'NONE', *, *, #1190, .T. ) ;
#4683=AXIS2_PLACEMENT_3D ( 'NONE', #7691, #7083, #1115 ) ;
#4691=DIRECTION ( 'NONE',  ( 0.000000000000000000, 0.000000000000000000, -1.000000000000000000 ) ) ;
#4695=DIRECTION ( 'NONE',  ( -1.000000000000000000, -8.881784197001244435E-16, 0.000000000000000000 ) ) ;
#4714=ORIENTED_EDGE ( 'NONE', *, *, #7195, .T. ) ;
#4746=CARTESIAN_POINT ( 'NONE',  ( 6.686525924292292977, -5.377136764700166438, -8.083279549040401690 ) ) ;
#4754=EDGE_CURVE ( 'NONE', #2122, #4141, #4364, .T. ) ;
#4758=EDGE_LOOP ( 'NONE', ( #1211, #2230, #839, #5512, #4792, #3418 ) ) ;
#4774=DIRECTION ( 'NONE',  ( -1.000000000000000000, -8.881784197001244435E-16, 0.000000000000000000 ) ) ;
#4778=AXIS2_PLACEMENT_3D ( 'NONE', #7107, #5182, #5662 ) ;
#4784=CARTESIAN_POINT ( 'NONE',  ( 0.000000000000000000, 0.000000000000000000, 0.000000000000000000 ) ) ;
#4792=ORIENTED_EDGE ( 'NONE', *, *, #3549, .F. ) ;
#4793=CARTESIAN_POINT ( 'NONE',  ( -8.000000000000664357, -1.555946510855795273, -0.06708870216369239303 ) ) ;
#4815=ORIENTED_EDGE ( 'NONE', *, *, #1608, .F. ) ;
#4833=EDGE_CURVE ( 'NONE', #4401, #2122, #7045, .T. ) ;
#4862=AXIS2_PLACEMENT_3D ( 'NONE', #1580, #8293, #6905 ) ;
#4866=DIRECTION ( 'NONE',  ( -0.000000000000000000, -0.000000000000000000, 1.000000000000000000 ) ) ;
#4867=B_SPLINE_CURVE_WITH_KNOTS ( 'NONE', 3,
 ( #613, #6115, #3263, #74, #5948, #6030 ),
 .UNSPECIFIED., .F., .F.,
 ( 4, 2, 4 ),
 ( 2.380731626810675838E-07, 0.002336973833157153513, 0.004673709593151625756 ),
 .UNSPECIFIED. ) ;
#4881=CARTESIAN_POINT ( 'NONE',  ( -8.000000000000673239, 4.618802153517287401, -7.685468820183672278 ) ) ;
#4902=ORIENTED_EDGE ( 'NONE', *, *, #3361, .F. ) ;
#4907=AXIS2_PLACEMENT_3D ( 'NONE', #5069, #1187, #4503 ) ;
#4928=CARTESIAN_POINT ( 'NONE',  ( -6.661338147750939243E-13, 9.237604307034352757, -0.7145311798163467287 ) ) ;
#4935=FACE_OUTER_BOUND ( 'NONE', #4526, .T. ) ;
#4936=EDGE_LOOP ( 'NONE', ( #726, #887 ) ) ;
#4958=ADVANCED_FACE ( 'NONE', ( #789 ), #6494, .T. ) ;
#4988=FACE_OUTER_BOUND ( 'NONE', #8110, .T. ) ;
#5009=B_SPLINE_CURVE_WITH_KNOTS ( 'NONE', 3,
 ( #3285, #725, #6015, #2772, #5967, #99, #6697, #6 ),
 .UNSPECIFIED., .F., .F.,
 ( 4, 2, 2, 4 ),
 ( 0.004673709593151410650, 0.005837709341827138597, 0.007001709090502865676, 0.009329708587854319835 ),
 .UNSPECIFIED. ) ;
#5030=DIRECTION ( 'NONE',  ( 1.000000000000000000, 8.881784197001244435E-16, 0.000000000000000000 ) ) ;
#5055=DIRECTION ( 'NONE',  ( 0.000000000000000000, 0.000000000000000000, 1.000000000000000000 ) ) ;
#5063=ORIENTED_EDGE ( 'NONE', *, *, #7094, .F. ) ;
#5069=CARTESIAN_POINT ( 'NONE',  ( 0.000000000000000000, 0.000000000000000000, -8.400000000000018119 ) ) ;
#5076=CARTESIAN_POINT ( 'NONE',  ( 8.000000000000012434, 0.7809653281576679484, -5.991911068876919021E-15 ) ) ;
#5078=VERTEX_POINT ( 'NONE', #597 ) ;
#5079=ORIENTED_EDGE ( 'NONE', *, *, #7102, .F. ) ;
#5080=ADVANCED_FACE ( 'NONE', ( #1379 ), #4438, .T. ) ;
#5087=CARTESIAN_POINT ( 'NONE',  ( -6.661338147750939243E-13, 9.237604307034352757, -7.685468820183672278 ) ) ;
#5093=VERTEX_POINT ( 'NONE', #5163 ) ;
#5096=CARTESIAN_POINT ( 'NONE',  ( 2.309976723937089194, -7.903938623646893369, -8.269346954796276350 ) ) ;
#5098=ADVANCED_FACE ( 'NONE', ( #8557 ), #4587, .T. ) ;
#5114=CARTESIAN_POINT ( 'NONE',  ( 8.000000000000007105, 4.618802153517065356, -0.7145311798163467287 ) ) ;
#5115=CARTESIAN_POINT ( 'NONE',  ( 8.000000000000012434, -1.555946510856071940, -8.332911297836661291 ) ) ;
#5116=ORIENTED_EDGE ( 'NONE', *, *, #3145, .F. ) ;
#5119=CARTESIAN_POINT ( 'NONE',  ( 8.000000000000008882, 3.871967595402188156, -7.901061386767544548 ) ) ;
#5127=AXIS2_PLACEMENT_3D ( 'NONE', #3509, #903, #6873 ) ;
#5163=CARTESIAN_POINT ( 'NONE',  ( 7.999999999999340972, -4.618802153516732290, -7.685468820183672278 ) ) ;
#5172=B_SPLINE_CURVE_WITH_KNOTS ( 'NONE', 3,
 ( #5882, #8504, #4420, #7726, #2545, #8543 ),
 .UNSPECIFIED., .F., .F.,
 ( 4, 2, 4 ),
 ( 2.380731628162083024E-07, 0.002336973833157790156, 0.004673709593152763735 ),
 .UNSPECIFIED. ) ;
#5175=CARTESIAN_POINT ( 'NONE',  ( 0.000000000000000000, 0.000000000000000000, 0.000000000000000000 ) ) ;
#5178=CARTESIAN_POINT ( 'NONE',  ( -4.440892098500626162E-13, -9.237604307034018802, -7.685468820183672278 ) ) ;
#5182=DIRECTION ( 'NONE',  ( 0.000000000000000000, 0.000000000000000000, 1.000000000000000000 ) ) ;
#5184=DIRECTION ( 'NONE',  ( 0.000000000000000000, 0.000000000000000000, 1.000000000000000000 ) ) ;
#5188=APPLICATION_CONTEXT ( 'automotive_design' ) ;
#5190=B_SPLINE_CURVE_WITH_KNOTS ( 'NONE', 3,
 ( #4491, #7677, #4369, #1180, #5096, #4451, #7031, #1097 ),
 .UNSPECIFIED., .F., .F.,
 ( 4, 2, 2, 4 ),
 ( 0.004673709593152784551, 0.005837709341828078817, 0.007001709090503373950, 0.009329708587853959012 ),
 .UNSPECIFIED. ) ;
#5201=FACE_OUTER_BOUND ( 'NONE', #4218, .T. ) ;
#5211=CARTESIAN_POINT ( 'NONE',  ( 8.000000000000015987, -3.098204225878034901, -8.084209322808163733 ) ) ;
#5216=ADVANCED_FACE ( 'NONE', ( #4935 ), #3680, .F. ) ;
#5229=CARTESIAN_POINT ( 'NONE',  ( -8.000000000000229150, -4.618802153516843312, -7.685468820183672278 ) ) ;
#5233=CIRCLE ( 'NONE', #221, 8.000000000000007105 ) ;
#5238=AXIS2_PLACEMENT_3D ( 'NONE', #7168, #1719, #2460 ) ;
#5243=( LENGTH_UNIT ( ) NAMED_UNIT ( * ) SI_UNIT ( .MILLI., .METRE. ) );
#5269=CARTESIAN_POINT ( 'NONE',  ( -4.000000000000003553, -6.928203230275431501, -8.400000000000018119 ) ) ;
#5273=EDGE_CURVE ( 'NONE', #2336, #4545, #6963, .T. ) ;
#5341=EDGE_CURVE ( 'NONE', #7519, #1856, #2854, .T. ) ;
#5345=B_SPLINE_CURVE_WITH_KNOTS ( 'NONE', 3,
 ( #434, #2556, #5211, #5115, #4394, #1239 ),
 .UNSPECIFIED., .F., .F.,
 ( 4, 2, 4 ),
 ( 0.008240550023493714918, 0.01057684187039402597, 0.01291313371729433702 ),
 .UNSPECIFIED. ) ;
#5362=CARTESIAN_POINT ( 'NONE',  ( -0.6543471694415565754, -8.859816792613557368, -7.903584543331262147 ) ) ;
#5376=B_SPLINE_CURVE_WITH_KNOTS ( 'NONE', 3,
 ( #7432, #1648, #1572, #3715, #6337, #3591, #2769, #4928 ),
 .UNSPECIFIED., .F., .F.,
 ( 4, 2, 2, 4 ),
 ( 0.004673709593151625756, 0.005837709341827240078, 0.007001709090502855268, 0.009329708587854083912 ),
 .UNSPECIFIED. ) ;
#5384=VERTEX_POINT ( 'NONE', #5087 ) ;
#5439=VERTEX_POINT ( 'NONE', #3780 ) ;
#5449=STYLED_ITEM('',(#8670),#56);
#5451=CARTESIAN_POINT ( 'NONE',  ( -3.660532965669703209, 7.124194613927820718, -8.399999999999687716 ) ) ;
#5473=CARTESIAN_POINT ( 'NONE',  ( 0.000000000000000000, 0.000000000000000000, -8.400999999999992696 ) ) ;
#5476=AXIS2_PLACEMENT_3D ( 'NONE', #7108, #7192, #1134 ) ;
#5477=AXIS2_PLACEMENT_3D ( 'NONE', #5840, #4300, #2506 ) ;
#5484=DIRECTION ( 'NONE',  ( 0.000000000000000000, 0.000000000000000000, -1.000000000000000000 ) ) ;
#5505=ORIENTED_EDGE ( 'NONE', *, *, #1912, .F. ) ;
#5512=ORIENTED_EDGE ( 'NONE', *, *, #7464, .F. ) ;
#5527=ORIENTED_EDGE ( 'NONE', *, *, #8507, .F. ) ;
#5530=B_SPLINE_CURVE_WITH_KNOTS ( 'NONE', 3,
 ( #156, #6837, #2177, #7486, #6194, #202, #8176, #3567 ),
 .UNSPECIFIED., .F., .F.,
 ( 4, 2, 2, 4 ),
 ( 0.004673709593152776745, 0.005837709341828072745, 0.007001709090503368746, 0.009329708587853959012 ),
 .UNSPECIFIED. ) ;
#5560=AXIS2_PLACEMENT_3D ( 'NONE', #3673, #5055, #1741 ) ;
#5567=AXIS2_PLACEMENT_3D ( 'NONE', #3253, #1902, #5937 ) ;
#5571=EDGE_CURVE ( 'NONE', #4545, #3409, #1525, .T. ) ;
#5574=EDGE_CURVE ( 'NONE', #4545, #2313, #5233, .T. ) ;
#5579=DIRECTION ( 'NONE',  ( -1.000000000000000000, -8.881784197001244435E-16, 0.000000000000000000 ) ) ;
#5588=EDGE_LOOP ( 'NONE', ( #7874, #2961, #5505, #6711, #6665, #8207 ) ) ;
#5612=DIRECTION ( 'NONE',  ( -0.000000000000000000, -0.000000000000000000, 1.000000000000000000 ) ) ;
#5619=ORIENTED_EDGE ( 'NONE', *, *, #6180, .T. ) ;
#5636=EDGE_LOOP ( 'NONE', ( #1521, #6640, #198 ) ) ;
#5654=CARTESIAN_POINT ( 'NONE',  ( 0.000000000000000000, 0.000000000000000000, -8.400000000000018119 ) ) ;
#5662=DIRECTION ( 'NONE',  ( -0.9237280213470678847, -0.3830490080632384942, 0.000000000000000000 ) ) ;
#5679=FACE_OUTER_BOUND ( 'NONE', #3037, .T. ) ;
#5717=CIRCLE ( 'NONE', #1931, 8.000000000000007105 ) ;
#5719=CARTESIAN_POINT ( 'NONE',  ( -8.000000000000673239, 4.618802153517287401, -7.685468820183672278 ) ) ;
#5722=CARTESIAN_POINT ( 'NONE',  ( 8.000000000000008882, 3.115336682267075386, -0.3193931313915240877 ) ) ;
#5755=CARTESIAN_POINT ( 'NONE',  ( -8.000000000000673239, 4.618802153517287401, -0.7145311798163467287 ) ) ;
#5784=CARTESIAN_POINT ( 'NONE',  ( -4.000000000000891731, 6.928203230275542523, 0.000000000000000000 ) ) ;
#5817=EDGE_LOOP ( 'NONE', ( #2868, #574, #6388, #6243, #4270, #2245 ) ) ;
#5821=EDGE_CURVE ( 'NONE', #5093, #6993, #4533, .T. ) ;
#5840=CARTESIAN_POINT ( 'NONE',  ( 0.000000000000000000, 0.000000000000000000, 0.000000000000000000 ) ) ;
#5862=CARTESIAN_POINT ( 'NONE',  ( -7.347286611337213280, -4.995646404165206889, -7.903039949738177583 ) ) ;
#5865=CARTESIAN_POINT ( 'NONE',  ( 0.000000000000000000, 0.000000000000000000, 0.000000000000000000 ) ) ;
#5875=AXIS2_PLACEMENT_3D ( 'NONE', #4784, #5484, #4695 ) ;
#5877=CARTESIAN_POINT ( 'NONE',  ( -8.000000000000229150, -4.618802153516843312, -7.685468820183672278 ) ) ;
#5882=CARTESIAN_POINT ( 'NONE',  ( -6.661338147750939243E-13, 9.237604307034352757, -0.7145311798163467287 ) ) ;
#5902=VERTEX_POINT ( 'NONE', #8393 ) ;
#5904=CIRCLE ( 'NONE', #4907, 8.000000000000007105 ) ;
#5908=CARTESIAN_POINT ( 'NONE',  ( -5.355005115541073835, -6.145890662064625865, -8.317753204360252894 ) ) ;
#5927=ADVANCED_FACE ( 'NONE', ( #470 ), #1809, .T. ) ;
#5936=ORIENTED_EDGE ( 'NONE', *, *, #5821, .T. ) ;
#5937=DIRECTION ( 'NONE',  ( -1.000000000000000000, -8.881784197001244435E-16, 0.000000000000000000 ) ) ;
#5942=ADVANCED_FACE ( 'NONE', ( #1938 ), #418, .T. ) ;
#5948=CARTESIAN_POINT ( 'NONE',  ( -4.681481898397863439, 6.534749472788354829, -3.895114889266789776E-13 ) ) ;
#5952=FACE_OUTER_BOUND ( 'NONE', #6117, .T. ) ;
#5961=CARTESIAN_POINT ( 'NONE',  ( 5.355005115540884653, 6.145890662064626753, -8.317753204360318620 ) ) ;
#5967=CARTESIAN_POINT ( 'NONE',  ( -5.690023276062574631, -5.952467836904122400, -0.1306530452038688617 ) ) ;
#5971=ORIENTED_EDGE ( 'NONE', *, *, #7429, .T. ) ;
#6015=CARTESIAN_POINT ( 'NONE',  ( -4.680456609904114273, -6.535341423375586878, -0.01688885742781164739 ) ) ;
#6023=CARTESIAN_POINT ( 'NONE',  ( -8.000000000000673239, 4.618802153517287401, -8.400000000000018119 ) ) ;
#6027=CARTESIAN_POINT ( 'NONE',  ( -3.318518101603130876, -7.321656987762883873, -8.399999999999986144 ) ) ;
#6030=CARTESIAN_POINT ( 'NONE',  ( -4.000000000000891731, 6.928203230275542523, 0.000000000000000000 ) ) ;
#6034=FACE_OUTER_BOUND ( 'NONE', #995, .T. ) ;
#6035=PLANE ( 'NONE',  #3086 ) ;
#6048=( NAMED_UNIT ( * ) SI_UNIT ( $, .STERADIAN. ) SOLID_ANGLE_UNIT ( ) );
#6063=CARTESIAN_POINT ( 'NONE',  ( -6.661338147750939243E-13, -9.237604307034130713, -8.400000000000018119 ) ) ;
#6075=CARTESIAN_POINT ( 'NONE',  ( -2.645508037662052558, -7.710219529346595380, -8.331901280394566456 ) ) ;
#6093=CARTESIAN_POINT ( 'NONE',  ( 7.347286611336940609, 4.995646404165252186, -7.903039949738288605 ) ) ;
#6095=DIRECTION ( 'NONE',  ( 0.000000000000000000, 0.000000000000000000, 1.000000000000000000 ) ) ;
#6101=CARTESIAN_POINT ( 'NONE',  ( -8.000000000000667910, 3.115336682267232593, -0.3193931313919167181 ) ) ;
#6115=CARTESIAN_POINT ( 'NONE',  ( -7.345652830559441071, 4.996589667937682222, -0.4964154566692197679 ) ) ;
#6117=EDGE_LOOP ( 'NONE', ( #3186, #3047, #7061 ) ) ;
#6146=AXIS2_PLACEMENT_3D ( 'NONE', #3611, #2297, #1044 ) ;
#6166=EDGE_CURVE ( 'NONE', #2122, #6377, #8277, .T. ) ;
#6180=EDGE_CURVE ( 'NONE', #2313, #4294, #5376, .T. ) ;
#6181=DIRECTION ( 'NONE',  ( -1.000000000000000000, -2.664535259100374908E-15, 0.000000000000000000 ) ) ;
#6185=CARTESIAN_POINT ( 'NONE',  ( 5.080504117408895404, 2.106769544347820489, -8.400999999999992696 ) ) ;
#6191=ADVANCED_FACE ( 'NONE', ( #767 ), #1827, .T. ) ;
#6194=CARTESIAN_POINT ( 'NONE',  ( 2.309976723937096743, -7.903938623646888928, -0.1306530452037402423 ) ) ;
#6228=CARTESIAN_POINT ( 'NONE',  ( -8.000000000000673239, 1.572549600175905171, -0.06894455525554724074 ) ) ;
#6239=CARTESIAN_POINT ( 'NONE',  ( 8.000000000000015987, -3.098204225878038010, -0.3157906771918544409 ) ) ;
#6243=ORIENTED_EDGE ( 'NONE', *, *, #8572, .F. ) ;
#6248=AXIS2_PLACEMENT_3D ( 'NONE', #2937, #5612, #6181 ) ;
#6252=CARTESIAN_POINT ( 'NONE',  ( 0.000000000000000000, 0.000000000000000000, -8.400000000000018119 ) ) ;
#6273=AXIS2_PLACEMENT_3D ( 'NONE', #895, #7033, #6345 ) ;
#6288=ADVANCED_FACE ( 'NONE', ( #5952 ), #8517, .T. ) ;
#6291=CARTESIAN_POINT ( 'NONE',  ( -6.686525924293513334, 5.377136764700441773, -8.083279549039747991 ) ) ;
#6296=B_SPLINE_CURVE_WITH_KNOTS ( 'NONE', 3,
 ( #4513, #1813, #7130, #1159, #3249, #3819 ),
 .UNSPECIFIED., .F., .F.,
 ( 4, 2, 4 ),
 ( 2.380731632781927508E-07, 0.002336973833158027380, 0.004673709593152776745 ),
 .UNSPECIFIED. ) ;
#6305=ORIENTED_EDGE ( 'NONE', *, *, #2083, .F. ) ;
#6337=CARTESIAN_POINT ( 'NONE',  ( -2.309976723938477416, 7.903938623647078998, -0.1306530452040687018 ) ) ;
#6345=DIRECTION ( 'NONE',  ( -0.9237280213470678847, -0.3830490080632384942, 0.000000000000000000 ) ) ;
#6352=ADVANCED_FACE ( 'NONE', ( #4443 ), #491, .T. ) ;
#6364=CARTESIAN_POINT ( 'NONE',  ( -1.313474075707481425, -8.479269695850799593, -0.3167204509598293694 ) ) ;
#6375=VERTEX_POINT ( 'NONE', #1174 ) ;
#6377=VERTEX_POINT ( 'NONE', #525 ) ;
#6386=EDGE_CURVE ( 'NONE', #5093, #5902, #3180, .T. ) ;
#6388=ORIENTED_EDGE ( 'NONE', *, *, #1480, .T. ) ;
#6393=ORIENTED_EDGE ( 'NONE', *, *, #6180, .F. ) ;
#6407=CARTESIAN_POINT ( 'NONE',  ( 8.000000000000008882, 1.572549600175701778, -8.331055444744873029 ) ) ;
#6454=CARTESIAN_POINT ( 'NONE',  ( 5.355005115540882876, 6.145890662064627641, -0.08224679563969784779 ) ) ;
#6460=DIRECTION ( 'NONE',  ( 0.000000000000000000, 0.000000000000000000, 1.000000000000000000 ) ) ;
#6475=CARTESIAN_POINT ( 'NONE',  ( -4.440892098500626162E-13, -9.237604307034018802, -7.685468820183672278 ) ) ;
#6481=CARTESIAN_POINT ( 'NONE',  ( 0.6543471694407191341, 8.859816792613939285, -7.903584543331081846 ) ) ;
#6482=ORIENTED_EDGE ( 'NONE', *, *, #8219, .F. ) ;
#6484=VERTEX_POINT ( 'NONE', #77 ) ;
#6492=CONICAL_SURFACE ( 'NONE', #7057, 8.000000000000007105, 1.047197551196597631 ) ;
#6494=CONICAL_SURFACE ( 'NONE', #4412, 8.000000000000007105, 1.047197551196597631 ) ;
#6498=ADVANCED_FACE ( 'NONE', ( #6034 ), #6872, .T. ) ;
#6504=DIRECTION ( 'NONE',  ( -0.5000000000000033307, -0.8660254037844367092, 0.000000000000000000 ) ) ;
#6538=VECTOR ( 'NONE', #7072, 1000.000000000000000 ) ;
#6542=DIRECTION ( 'NONE',  ( -0.000000000000000000, -0.000000000000000000, 1.000000000000000000 ) ) ;
#6552=B_SPLINE_CURVE_WITH_KNOTS ( 'NONE', 3,
 ( #2563, #395, #6407, #8441, #5119, #1864 ),
 .UNSPECIFIED., .F., .F.,
 ( 4, 2, 4 ),
 ( 0.01291313371729433702, 0.01525081363757292696, 0.01758849355785151516 ),
 .UNSPECIFIED. ) ;
#6568=EDGE_CURVE ( 'NONE', #8133, #5078, #2235, .T. ) ;
#6640=ORIENTED_EDGE ( 'NONE', *, *, #3356, .T. ) ;
#6664=CARTESIAN_POINT ( 'NONE',  ( -8.000000000000229150, 4.440892098500626162E-13, 0.000000000000000000 ) ) ;
#6665=ORIENTED_EDGE ( 'NONE', *, *, #2119, .F. ) ;
#6666=ADVANCED_FACE ( 'NONE', ( #3666 ), #4014, .T. ) ;
#6670=DIRECTION ( 'NONE',  ( 0.000000000000000000, 0.000000000000000000, 1.000000000000000000 ) ) ;
#6697=CARTESIAN_POINT ( 'NONE',  ( -7.347286611337208839, -4.995646404165207777, -0.4969600502618418680 ) ) ;
#6711=ORIENTED_EDGE ( 'NONE', *, *, #2331, .F. ) ;
#6718=EDGE_CURVE ( 'NONE', #5384, #1589, #677, .T. ) ;
#6732=SHAPE_REPRESENTATION_RELATIONSHIP ( 'NONE' , 'NONE' ,  #2397, #1361 ) ;
#6740=FACE_OUTER_BOUND ( 'NONE', #7898, .T. ) ;
#6751=EDGE_CURVE ( 'NONE', #2336, #4141, #5009, .T. ) ;
#6754=CARTESIAN_POINT ( 'NONE',  ( 3.999999999999337419, -6.928203230275431501, -8.400000000000018119 ) ) ;
#6771=ORIENTED_EDGE ( 'NONE', *, *, #4833, .T. ) ;
#6776=CARTESIAN_POINT ( 'NONE',  ( 4.000000000000003553, 6.928203230275431501, 0.000000000000000000 ) ) ;
#6837=CARTESIAN_POINT ( 'NONE',  ( 3.660532965668319427, -7.124194613927638642, 1.269962144704687948E-13 ) ) ;
#6860=DIRECTION ( 'NONE',  ( -1.000000000000000000, -8.881784197001244435E-16, 0.000000000000000000 ) ) ;
#6872=CONICAL_SURFACE ( 'NONE', #3098, 8.000000000000007105, 1.047197551196597631 ) ;
#6873=DIRECTION ( 'NONE',  ( -1.000000000000000000, -8.881784197001244435E-16, 0.000000000000000000 ) ) ;
#6905=DIRECTION ( 'NONE',  ( -1.000000000000000000, -8.881784197001244435E-16, 0.000000000000000000 ) ) ;
#6906=AXIS2_PLACEMENT_3D ( 'NONE', #289, #4866, #7528 ) ;
#6910=DIRECTION ( 'NONE',  ( -0.9237280213470678847, -0.3830490080632384942, 0.000000000000000000 ) ) ;
#6931=CARTESIAN_POINT ( 'NONE',  ( 7.999999999999340972, -4.618802153516732290, -0.7145311798163467287 ) ) ;
#6963=CIRCLE ( 'NONE', #4862, 8.000000000000007105 ) ;
#6978=ORIENTED_EDGE ( 'NONE', *, *, #5571, .T. ) ;
#6988=CARTESIAN_POINT ( 'NONE',  ( 4.000000000000003553, 6.928203230275431501, 0.000000000000000000 ) ) ;
#6993=VERTEX_POINT ( 'NONE', #2996 ) ;
#7028=DIRECTION ( 'NONE',  ( 0.5000000000000035527, 0.8660254037844365982, 0.000000000000000000 ) ) ;
#7031=CARTESIAN_POINT ( 'NONE',  ( 0.6527133886625579029, -8.860760056385743155, -7.903039949738283276 ) ) ;
#7033=DIRECTION ( 'NONE',  ( 0.000000000000000000, 0.000000000000000000, 1.000000000000000000 ) ) ;
#7045=B_SPLINE_CURVE_WITH_KNOTS ( 'NONE', 3,
 ( #5269, #523, #2664, #5908, #8533, #3177, #5862, #5229 ),
 .UNSPECIFIED., .F., .F.,
 ( 4, 2, 2, 4 ),
 ( 0.004673709593151418457, 0.005837709341827142066, 0.007001709090502865676, 0.009329708587854312896 ),
 .UNSPECIFIED. ) ;
#7057=AXIS2_PLACEMENT_3D ( 'NONE', #3506, #281, #4774 ) ;
#7061=ORIENTED_EDGE ( 'NONE', *, *, #1480, .F. ) ;
#7072=DIRECTION ( 'NONE',  ( 0.000000000000000000, 0.000000000000000000, 1.000000000000000000 ) ) ;
#7079=ORIENTED_EDGE ( 'NONE', *, *, #4404, .T. ) ;
#7083=DIRECTION ( 'NONE',  ( -1.000000000000000000, -8.881784197001244435E-16, 0.000000000000000000 ) ) ;
#7094=EDGE_CURVE ( 'NONE', #2959, #4132, #3467, .T. ) ;
#7102=EDGE_CURVE ( 'NONE', #7519, #2870, #2962, .T. ) ;
#7107=CARTESIAN_POINT ( 'NONE',  ( 0.000000000000000000, 0.000000000000000000, 0.000000000000000000 ) ) ;
#7108=CARTESIAN_POINT ( 'NONE',  ( -6.661338147750939243E-13, -9.237604307034130713, -8.400000000000018119 ) ) ;
#7130=CARTESIAN_POINT ( 'NONE',  ( 6.686525924292292977, -5.377136764700166438, -0.3167204509596151518 ) ) ;
#7153=ORIENTED_EDGE ( 'NONE', *, *, #2667, .T. ) ;
#7156=CARTESIAN_POINT ( 'NONE',  ( -2.309976723938476972, 7.903938623647078998, -8.269346954795947724 ) ) ;
#7163=PRODUCT_DEFINITION_SHAPE ( 'NONE', 'NONE',  #7643 ) ;
#7168=CARTESIAN_POINT ( 'NONE',  ( 0.000000000000000000, 0.000000000000000000, -8.400000000000018119 ) ) ;
#7170=CARTESIAN_POINT ( 'NONE',  ( 8.000000000000008882, 3.871967595402187268, -0.4989386132324758472 ) ) ;
#7176=CARTESIAN_POINT ( 'NONE',  ( 0.000000000000000000, 0.000000000000000000, 0.000000000000000000 ) ) ;
#7192=DIRECTION ( 'NONE',  ( 0.5000000000000029976, -0.8660254037844370423, 0.000000000000000000 ) ) ;
#7195=EDGE_CURVE ( 'NONE', #6375, #2336, #1698, .T. ) ;
#7201=FACE_BOUND ( 'NONE', #4936, .T. ) ;
#7204=CARTESIAN_POINT ( 'NONE',  ( -8.000000000000007105, -4.618802153517065356, -8.400000000000018119 ) ) ;
#7215=ORIENTED_EDGE ( 'NONE', *, *, #3145, .T. ) ;
#7245=ORIENTED_EDGE ( 'NONE', *, *, #6386, .F. ) ;
#7254=AXIS2_PLACEMENT_3D ( 'NONE', #6252, #7585, #3425 ) ;
#7262=ORIENTED_EDGE ( 'NONE', *, *, #2767, .F. ) ;
#7272=ORIENTED_EDGE ( 'NONE', *, *, #8572, .T. ) ;
#7279=DIRECTION ( 'NONE',  ( 1.000000000000000000, 8.881784197001244435E-16, 0.000000000000000000 ) ) ;
#7366=B_SPLINE_CURVE_WITH_KNOTS ( 'NONE', 3,
 ( #3981, #7993, #4024, #5961, #2021, #3322, #6093, #3277 ),
 .UNSPECIFIED., .F., .F.,
 ( 4, 2, 2, 4 ),
 ( 0.004673709593152765469, 0.005837709341828116114, 0.007001709090503465890, 0.009329708587854167179 ),
 .UNSPECIFIED. ) ;
#7373=CARTESIAN_POINT ( 'NONE',  ( -6.661338147750939243E-13, 9.237604307034352757, -8.400000000000018119 ) ) ;
#7382=CARTESIAN_POINT ( 'NONE',  ( -8.000000000000229150, -4.618802153516843312, -0.7145311798163467287 ) ) ;
#7383=DIRECTION ( 'NONE',  ( -0.8660254037844362651, -0.5000000000000039968, 0.000000000000000000 ) ) ;
#7388=EDGE_LOOP ( 'NONE', ( #5936, #3989, #3902 ) ) ;
#7392=CARTESIAN_POINT ( 'NONE',  ( 4.681481898396449459, -6.534749472788188740, -8.400000000000190425 ) ) ;
#7396=CARTESIAN_POINT ( 'NONE',  ( -2.644994884460001749, 7.710515798486560435, -8.317753204360025521 ) ) ;
#7417=EDGE_CURVE ( 'NONE', #1856, #2336, #8468, .T. ) ;
#7429=EDGE_CURVE ( 'NONE', #2959, #3453, #3558, .T. ) ;
#7432=CARTESIAN_POINT ( 'NONE',  ( -4.000000000000891731, 6.928203230275542523, 0.000000000000000000 ) ) ;
#7442=PRODUCT_DEFINITION_FORMATION_WITH_SPECIFIED_SOURCE ( 'ANY', '', #1050, .NOT_KNOWN. ) ;
#7452=CARTESIAN_POINT ( 'NONE',  ( -8.000000000000669687, -0.7805016046286902265, -3.591589102947684298E-13 ) ) ;
#7464=EDGE_CURVE ( 'NONE', #5439, #2870, #4121, .T. ) ;
#7478=DIRECTION ( 'NONE',  ( 0.000000000000000000, 0.000000000000000000, 1.000000000000000000 ) ) ;
#7486=CARTESIAN_POINT ( 'NONE',  ( 2.644994884458586881, -7.710515798486395234, -0.08224679563963162299 ) ) ;
#7496=CARTESIAN_POINT ( 'NONE',  ( -4.681481898397863439, 6.534749472788354829, -8.399999999999629097 ) ) ;
#7519=VERTEX_POINT ( 'NONE', #990 ) ;
#7528=DIRECTION ( 'NONE',  ( -1.000000000000000000, -8.881784197001244435E-16, 0.000000000000000000 ) ) ;
#7533=CARTESIAN_POINT ( 'NONE',  ( 8.000000000000015987, -3.867591403078991519, -0.4976753153245472294 ) ) ;
#7544=CARTESIAN_POINT ( 'NONE',  ( -8.000000000000229150, 4.440892098500626162E-13, 0.000000000000000000 ) ) ;
#7563=AXIS2_PLACEMENT_3D ( 'NONE', #4203, #7478, #3512 ) ;
#7584=B_SPLINE_CURVE_WITH_KNOTS ( 'NONE', 3,
 ( #6931, #7533, #6239, #4349, #914, #1083 ),
 .UNSPECIFIED., .F., .F.,
 ( 4, 2, 4 ),
 ( 0.008240550023493711448, 0.01057684187039402424, 0.01291313371729433702 ),
 .UNSPECIFIED. ) ;
#7585=DIRECTION ( 'NONE',  ( 0.000000000000000000, 0.000000000000000000, 1.000000000000000000 ) ) ;
#7586=CARTESIAN_POINT ( 'NONE',  ( 4.339467034331170758, 6.732211846623375351, 1.758122761144706510E-14 ) ) ;
#7604=B_SPLINE_CURVE_WITH_KNOTS ( 'NONE', 3,
 ( #469, #3073, #3032, #8350, #3160, #5719 ),
 .UNSPECIFIED., .F., .F.,
 ( 4, 2, 4 ),
 ( 0.01291313371729497193, 0.01525081363757335370, 0.01758849355785173721 ),
 .UNSPECIFIED. ) ;
#7631=FACE_OUTER_BOUND ( 'NONE', #1491, .T. ) ;
#7643=PRODUCT_DEFINITION ( 'UNKNOWN', '', #7442, #540 ) ;
#7677=CARTESIAN_POINT ( 'NONE',  ( 3.660532965668318983, -7.124194613927635089, -8.400000000000146017 ) ) ;
#7691=CARTESIAN_POINT ( 'NONE',  ( -8.000000000000673239, 4.618802153517287401, -8.400000000000018119 ) ) ;
#7698=ORIENTED_EDGE ( 'NONE', *, *, #8462, .T. ) ;
#7716=AXIS2_PLACEMENT_3D ( 'NONE', #5175, #4359, #1869 ) ;
#7724=ADVANCED_FACE ( 'NONE', ( #7201, #3319 ), #8541, .T. ) ;
#7726=CARTESIAN_POINT ( 'NONE',  ( 2.645508037661678191, 7.710219529346706402, -0.06809871960543743830 ) ) ;
#7738=CARTESIAN_POINT ( 'NONE',  ( 5.080504117408889186, 2.106769544347817824, -8.400000000000018119 ) ) ;
#7765=ORIENTED_EDGE ( 'NONE', *, *, #4754, .T. ) ;
#7773=CARTESIAN_POINT ( 'NONE',  ( 8.000000000000007105, 0.000000000000000000, 0.000000000000000000 ) ) ;
#7782=AXIS2_PLACEMENT_3D ( 'NONE', #7373, #4543, #4065 ) ;
#7812=CARTESIAN_POINT ( 'NONE',  ( 0.000000000000000000, 0.000000000000000000, 0.000000000000000000 ) ) ;
#7847=ORIENTED_EDGE ( 'NONE', *, *, #2475, .F. ) ;
#7869=CIRCLE ( 'NONE', #6906, 8.000000000000007105 ) ;
#7874=ORIENTED_EDGE ( 'NONE', *, *, #1345, .F. ) ;
#7898=EDGE_LOOP ( 'NONE', ( #2564, #2162, #547, #3305 ) ) ;
#7903=CARTESIAN_POINT ( 'NONE',  ( -6.661338147750939243E-13, 9.237604307034352757, -8.400000000000018119 ) ) ;
#7917=ORIENTED_EDGE ( 'NONE', *, *, #6751, .T. ) ;
#7919=VECTOR ( 'NONE', #858, 1000.000000000000000 ) ;
#7920=CARTESIAN_POINT ( 'NONE',  ( -4.000000000000003553, -6.928203230275431501, -8.400000000000018119 ) ) ;
#7980=ORIENTED_EDGE ( 'NONE', *, *, #7102, .T. ) ;
#7993=CARTESIAN_POINT ( 'NONE',  ( 4.339467034331171646, 6.732211846623375351, -8.400000000000034106 ) ) ;
#8004=DIRECTION ( 'NONE',  ( -1.000000000000000000, -8.881784197001244435E-16, 0.000000000000000000 ) ) ;
#8037=ORIENTED_EDGE ( 'NONE', *, *, #3041, .T. ) ;
#8078=ORIENTED_EDGE ( 'NONE', *, *, #5341, .F. ) ;
#8096=ADVANCED_FACE ( 'NONE', ( #7631 ), #2657, .T. ) ;
#8108=CARTESIAN_POINT ( 'NONE',  ( 0.000000000000000000, 0.000000000000000000, -8.400000000000018119 ) ) ;
#8110=EDGE_LOOP ( 'NONE', ( #7765, #1913, #6978, #6482, #8527, #2669 ) ) ;
#8114=VECTOR ( 'NONE', #5184, 1000.000000000000000 ) ;
#8119=ADVANCED_FACE ( 'NONE', ( #974 ), #2973, .T. ) ;
#8133=VERTEX_POINT ( 'NONE', #451 ) ;
#8148=DIRECTION ( 'NONE',  ( 1.000000000000000000, 8.881784197001244435E-16, 0.000000000000000000 ) ) ;
#8176=CARTESIAN_POINT ( 'NONE',  ( 0.6527133886625599013, -8.860760056385744932, -0.4969600502617356197 ) ) ;
#8187=DIRECTION ( 'NONE',  ( 0.000000000000000000, 0.000000000000000000, 1.000000000000000000 ) ) ;
#8207=ORIENTED_EDGE ( 'NONE', *, *, #2527, .F. ) ;
#8219=EDGE_CURVE ( 'NONE', #8133, #3409, #4091, .T. ) ;
#8227=DIRECTION ( 'NONE',  ( 0.000000000000000000, 0.000000000000000000, 1.000000000000000000 ) ) ;
#8243=CARTESIAN_POINT ( 'NONE',  ( -8.000000000000667910, -0.7805016046286897824, -8.399999999999657518 ) ) ;
#8248=EDGE_CURVE ( 'NONE', #5078, #5384, #4386, .T. ) ;
#8277=B_SPLINE_CURVE_WITH_KNOTS ( 'NONE', 3,
 ( #8325, #4076, #1691, #3634, #8243, #4365 ),
 .UNSPECIFIED., .F., .F.,
 ( 4, 2, 4 ),
 ( 0.008240550023493664611, 0.01057684187039431740, 0.01291313371729497193 ),
 .UNSPECIFIED. ) ;
#8290=DIRECTION ( 'NONE',  ( 0.000000000000000000, 0.000000000000000000, 1.000000000000000000 ) ) ;
#8293=DIRECTION ( 'NONE',  ( 0.000000000000000000, 0.000000000000000000, -1.000000000000000000 ) ) ;
#8317=ADVANCED_FACE ( 'NONE', ( #3522, #5679 ), #2256, .F. ) ;
#8325=CARTESIAN_POINT ( 'NONE',  ( -8.000000000000229150, -4.618802153516843312, -7.685468820183672278 ) ) ;
#8341=AXIS2_PLACEMENT_3D ( 'NONE', #1533, #4189, #6860 ) ;
#8350=CARTESIAN_POINT ( 'NONE',  ( -8.000000000000671463, 3.115336682267233481, -8.080606868608098736 ) ) ;
#8353=DIRECTION ( 'NONE',  ( 0.9237280213470678847, 0.3830490080632384942, 0.000000000000000000 ) ) ;
#8393=CARTESIAN_POINT ( 'NONE',  ( 7.999999999999340972, -4.618802153516732290, -0.7145311798163467287 ) ) ;
#8401=AXIS2_PLACEMENT_3D ( 'NONE', #3553, #6095, #4071 ) ;
#8415=VECTOR ( 'NONE', #6460, 1000.000000000000000 ) ;
#8417=CARTESIAN_POINT ( 'NONE',  ( -4.000000000000003553, -6.928203230275431501, 0.000000000000000000 ) ) ;
#8441=CARTESIAN_POINT ( 'NONE',  ( 8.000000000000008882, 3.115336682267075830, -8.080606868608489535 ) ) ;
#8462=EDGE_CURVE ( 'NONE', #5093, #6484, #5345, .T. ) ;
#8463=CARTESIAN_POINT ( 'NONE',  ( 5.080504117408889186, 2.106769544347817824, 0.000000000000000000 ) ) ;
#8468=CIRCLE ( 'NONE', #5127, 8.000000000000007105 ) ;
#8504=CARTESIAN_POINT ( 'NONE',  ( 0.6543471694407195782, 8.859816792613939285, -0.4964154566689378267 ) ) ;
#8507=EDGE_CURVE ( 'NONE', #5902, #1856, #6296, .T. ) ;
#8513=VERTEX_POINT ( 'NONE', #6475 ) ;
#8517=CONICAL_SURFACE ( 'NONE', #1983, 8.000000000000007105, 1.047197551196597631 ) ;
#8518=CIRCLE ( 'NONE', #4778, 5.500000000000023981 ) ;
#8524=CARTESIAN_POINT ( 'NONE',  ( 2.645508037661676859, 7.710219529346706402, -8.331901280394584219 ) ) ;
#8527=ORIENTED_EDGE ( 'NONE', *, *, #1594, .F. ) ;
#8533=CARTESIAN_POINT ( 'NONE',  ( -5.690023276062584401, -5.952467836904117959, -8.269346954796148452 ) ) ;
#8541=PLANE ( 'NONE',  #7782 ) ;
#8543=CARTESIAN_POINT ( 'NONE',  ( 4.000000000000003553, 6.928203230275431501, 0.000000000000000000 ) ) ;
#8550=DIRECTION ( 'NONE',  ( -0.5000000000000041078, 0.8660254037844363761, 0.000000000000000000 ) ) ;
#8557=FACE_OUTER_BOUND ( 'NONE', #2737, .T. ) ;
#8567=ORIENTED_EDGE ( 'NONE', *, *, #8219, .T. ) ;
#8569=CARTESIAN_POINT ( 'NONE',  ( -1.313474075707481648, -8.479269695850799593, -8.083279549040190304 ) ) ;
#8572=EDGE_CURVE ( 'NONE', #8513, #6375, #1428, .T. ) ;
#8583=DIRECTION ( 'NONE',  ( -1.000000000000000000, -1.776356839400249676E-15, 0.000000000000000000 ) ) ;
#8664=COLOUR_RGB('Black',0.12,0.14,0.17);
#8665=FILL_AREA_STYLE_COLOUR('',#8664);
#8666=FILL_AREA_STYLE('',(#8665));
#8667=SURFACE_STYLE_FILL_AREA(#8666);
#8668=SURFACE_SIDE_STYLE('',(#8667));
#8669=SURFACE_STYLE_USAGE(.BOTH.,#8668);
#8670=PRESENTATION_STYLE_ASSIGNMENT((#8669));
ENDSEC;
END-ISO-10303-21;
